ISO-10303-21;
HEADER;
/* Generated by software containing ST-Developer
 * from STEP Tools, Inc. (www.steptools.com) 
 */

FILE_DESCRIPTION(
/* description */ ('STEP AP214'),
/* implementation_level */ '2;1');

FILE_NAME(
/* name */ 'Socket Head Cap Screw M6x20.step',
/* time_stamp */ '2026-11-15T14:55:55-08:00',
/* author */ (''),
/* organization */ (''),
/* preprocessor_version */ 'ST-DEVELOPER v20.2',
/* originating_system */ 'Autodesk Translation Framework v15.17.0.0',
/* authorisation */ '');

FILE_SCHEMA (('AUTOMOTIVE_DESIGN { 1 0 10303 214 3 1 1 }'));
ENDSEC;

DATA;
#10=MECHANICAL_DESIGN_GEOMETRIC_PRESENTATION_REPRESENTATION('',(#961),#57079);
#895=SHAPE_REPRESENTATION_RELATIONSHIP('SRR','None',#57285,#924);
#924=ADVANCED_BREP_SHAPE_REPRESENTATION('',(#998),#57077);
#961=STYLED_ITEM('',(#57444),#998);
#998=MANIFOLD_SOLID_BREP('Body1',#24561);
#1338=FACE_BOUND('',#5225,.T.);
#1339=FACE_BOUND('',#5227,.T.);
#2085=PLANE('',#27382);
#2086=PLANE('',#27383);
#2087=PLANE('',#27384);
#2088=PLANE('',#27385);
#2089=PLANE('',#27386);
#2090=PLANE('',#27387);
#2091=PLANE('',#27388);
#2092=PLANE('',#27389);
#2093=PLANE('',#27390);
#2094=PLANE('',#27391);
#2155=CONICAL_SURFACE('',#27374,5.,0.785398163397445);
#2156=CONICAL_SURFACE('',#27376,2.4585,0.785398163397448);
#3506=FACE_OUTER_BOUND('',#5219,.T.);
#3507=FACE_OUTER_BOUND('',#5220,.T.);
#3508=FACE_OUTER_BOUND('',#5221,.T.);
#3509=FACE_OUTER_BOUND('',#5222,.T.);
#3510=FACE_OUTER_BOUND('',#5223,.T.);
#3511=FACE_OUTER_BOUND('',#5224,.T.);
#3512=FACE_OUTER_BOUND('',#5226,.T.);
#3513=FACE_OUTER_BOUND('',#5228,.T.);
#3514=FACE_OUTER_BOUND('',#5229,.T.);
#3515=FACE_OUTER_BOUND('',#5230,.T.);
#3516=FACE_OUTER_BOUND('',#5231,.T.);
#3517=FACE_OUTER_BOUND('',#5232,.T.);
#3518=FACE_OUTER_BOUND('',#5233,.T.);
#3519=FACE_OUTER_BOUND('',#5234,.T.);
#5219=EDGE_LOOP('',(#22626,#22627,#22628,#22629));
#5220=EDGE_LOOP('',(#22630,#22631,#22632,#22633));
#5221=EDGE_LOOP('',(#22634,#22635,#22636,#22637,#22638));
#5222=EDGE_LOOP('',(#22639,#22640,#22641,#22642,#22643));
#5223=EDGE_LOOP('',(#22644));
#5224=EDGE_LOOP('',(#22645));
#5225=EDGE_LOOP('',(#22646,#22647,#22648,#22649,#22650,#22651));
#5226=EDGE_LOOP('',(#22652));
#5227=EDGE_LOOP('',(#22653));
#5228=EDGE_LOOP('',(#22654,#22655,#22656,#22657));
#5229=EDGE_LOOP('',(#22658,#22659,#22660,#22661));
#5230=EDGE_LOOP('',(#22662,#22663,#22664,#22665));
#5231=EDGE_LOOP('',(#22666,#22667,#22668,#22669));
#5232=EDGE_LOOP('',(#22670,#22671,#22672,#22673));
#5233=EDGE_LOOP('',(#22674,#22675,#22676,#22677));
#5234=EDGE_LOOP('',(#22678,#22679,#22680,#22681,#22682,#22683));
#7174=LINE('',#56818,#9141);
#7175=LINE('',#56822,#9142);
#7176=LINE('',#56829,#9143);
#7177=LINE('',#56834,#9144);
#7178=LINE('',#56840,#9145);
#7179=LINE('',#56842,#9146);
#7180=LINE('',#56844,#9147);
#7181=LINE('',#56846,#9148);
#7182=LINE('',#56848,#9149);
#7183=LINE('',#56849,#9150);
#7184=LINE('',#56853,#9151);
#7185=LINE('',#56855,#9152);
#7186=LINE('',#56856,#9153);
#7187=LINE('',#56859,#9154);
#7188=LINE('',#56860,#9155);
#7189=LINE('',#56863,#9156);
#7190=LINE('',#56864,#9157);
#7191=LINE('',#56867,#9158);
#7192=LINE('',#56868,#9159);
#7193=LINE('',#56871,#9160);
#7194=LINE('',#56872,#9161);
#7195=LINE('',#56874,#9162);
#9141=VECTOR('',#34380,5.);
#9142=VECTOR('',#34385,5.);
#9143=VECTOR('',#34392,2.4585);
#9144=VECTOR('',#34399,3.);
#9145=VECTOR('',#34406,1000.);
#9146=VECTOR('',#34407,1000.);
#9147=VECTOR('',#34408,1000.);
#9148=VECTOR('',#34409,1000.);
#9149=VECTOR('',#34410,1000.);
#9150=VECTOR('',#34411,1000.);
#9151=VECTOR('',#34416,1000.);
#9152=VECTOR('',#34417,1000.);
#9153=VECTOR('',#34418,1000.);
#9154=VECTOR('',#34421,1000.);
#9155=VECTOR('',#34422,1000.);
#9156=VECTOR('',#34425,1000.);
#9157=VECTOR('',#34426,1000.);
#9158=VECTOR('',#34429,1000.);
#9159=VECTOR('',#34430,1000.);
#9160=VECTOR('',#34433,1000.);
#9161=VECTOR('',#34434,1000.);
#9162=VECTOR('',#34437,1000.);
#10265=CIRCLE('',#27372,5.);
#10266=CIRCLE('',#27373,5.);
#10267=CIRCLE('',#27375,4.4);
#10268=CIRCLE('',#27377,3.);
#10269=CIRCLE('',#27378,2.4585);
#10270=CIRCLE('',#27379,3.);
#10271=CIRCLE('',#27381,3.);
#12465=VERTEX_POINT('',#56815);
#12466=VERTEX_POINT('',#56817);
#12467=VERTEX_POINT('',#56821);
#12468=VERTEX_POINT('',#56825);
#12469=VERTEX_POINT('',#56826);
#12470=VERTEX_POINT('',#56828);
#12471=VERTEX_POINT('',#56833);
#12472=VERTEX_POINT('',#56838);
#12473=VERTEX_POINT('',#56839);
#12474=VERTEX_POINT('',#56841);
#12475=VERTEX_POINT('',#56843);
#12476=VERTEX_POINT('',#56845);
#12477=VERTEX_POINT('',#56847);
#12478=VERTEX_POINT('',#56852);
#12479=VERTEX_POINT('',#56854);
#12480=VERTEX_POINT('',#56858);
#12481=VERTEX_POINT('',#56862);
#12482=VERTEX_POINT('',#56866);
#12483=VERTEX_POINT('',#56870);
#15858=EDGE_CURVE('',#12465,#12465,#10265,.T.);
#15859=EDGE_CURVE('',#12465,#12466,#7174,.T.);
#15860=EDGE_CURVE('',#12466,#12466,#10266,.T.);
#15861=EDGE_CURVE('',#12466,#12467,#7175,.T.);
#15862=EDGE_CURVE('',#12467,#12467,#10267,.T.);
#15863=EDGE_CURVE('',#12468,#12469,#10268,.T.);
#15864=EDGE_CURVE('',#12469,#12470,#7176,.T.);
#15865=EDGE_CURVE('',#12470,#12470,#10269,.T.);
#15866=EDGE_CURVE('',#12469,#12468,#10270,.T.);
#15867=EDGE_CURVE('',#12468,#12471,#7177,.T.);
#15868=EDGE_CURVE('',#12471,#12471,#10271,.T.);
#15869=EDGE_CURVE('',#12472,#12473,#7178,.T.);
#15870=EDGE_CURVE('',#12474,#12472,#7179,.T.);
#15871=EDGE_CURVE('',#12475,#12474,#7180,.T.);
#15872=EDGE_CURVE('',#12476,#12475,#7181,.T.);
#15873=EDGE_CURVE('',#12477,#12476,#7182,.T.);
#15874=EDGE_CURVE('',#12473,#12477,#7183,.T.);
#15875=EDGE_CURVE('',#12478,#12473,#7184,.T.);
#15876=EDGE_CURVE('',#12479,#12478,#7185,.T.);
#15877=EDGE_CURVE('',#12479,#12472,#7186,.T.);
#15878=EDGE_CURVE('',#12480,#12479,#7187,.T.);
#15879=EDGE_CURVE('',#12480,#12474,#7188,.T.);
#15880=EDGE_CURVE('',#12481,#12480,#7189,.T.);
#15881=EDGE_CURVE('',#12481,#12475,#7190,.T.);
#15882=EDGE_CURVE('',#12482,#12481,#7191,.T.);
#15883=EDGE_CURVE('',#12482,#12476,#7192,.T.);
#15884=EDGE_CURVE('',#12483,#12482,#7193,.T.);
#15885=EDGE_CURVE('',#12483,#12477,#7194,.T.);
#15886=EDGE_CURVE('',#12478,#12483,#7195,.T.);
#22626=ORIENTED_EDGE('',*,*,#15858,.F.);
#22627=ORIENTED_EDGE('',*,*,#15859,.T.);
#22628=ORIENTED_EDGE('',*,*,#15860,.T.);
#22629=ORIENTED_EDGE('',*,*,#15859,.F.);
#22630=ORIENTED_EDGE('',*,*,#15860,.F.);
#22631=ORIENTED_EDGE('',*,*,#15861,.T.);
#22632=ORIENTED_EDGE('',*,*,#15862,.T.);
#22633=ORIENTED_EDGE('',*,*,#15861,.F.);
#22634=ORIENTED_EDGE('',*,*,#15863,.T.);
#22635=ORIENTED_EDGE('',*,*,#15864,.T.);
#22636=ORIENTED_EDGE('',*,*,#15865,.F.);
#22637=ORIENTED_EDGE('',*,*,#15864,.F.);
#22638=ORIENTED_EDGE('',*,*,#15866,.T.);
#22639=ORIENTED_EDGE('',*,*,#15863,.F.);
#22640=ORIENTED_EDGE('',*,*,#15867,.T.);
#22641=ORIENTED_EDGE('',*,*,#15868,.T.);
#22642=ORIENTED_EDGE('',*,*,#15867,.F.);
#22643=ORIENTED_EDGE('',*,*,#15866,.F.);
#22644=ORIENTED_EDGE('',*,*,#15865,.T.);
#22645=ORIENTED_EDGE('',*,*,#15862,.F.);
#22646=ORIENTED_EDGE('',*,*,#15869,.F.);
#22647=ORIENTED_EDGE('',*,*,#15870,.F.);
#22648=ORIENTED_EDGE('',*,*,#15871,.F.);
#22649=ORIENTED_EDGE('',*,*,#15872,.F.);
#22650=ORIENTED_EDGE('',*,*,#15873,.F.);
#22651=ORIENTED_EDGE('',*,*,#15874,.F.);
#22652=ORIENTED_EDGE('',*,*,#15858,.T.);
#22653=ORIENTED_EDGE('',*,*,#15868,.F.);
#22654=ORIENTED_EDGE('',*,*,#15869,.T.);
#22655=ORIENTED_EDGE('',*,*,#15875,.F.);
#22656=ORIENTED_EDGE('',*,*,#15876,.F.);
#22657=ORIENTED_EDGE('',*,*,#15877,.T.);
#22658=ORIENTED_EDGE('',*,*,#15870,.T.);
#22659=ORIENTED_EDGE('',*,*,#15877,.F.);
#22660=ORIENTED_EDGE('',*,*,#15878,.F.);
#22661=ORIENTED_EDGE('',*,*,#15879,.T.);
#22662=ORIENTED_EDGE('',*,*,#15871,.T.);
#22663=ORIENTED_EDGE('',*,*,#15879,.F.);
#22664=ORIENTED_EDGE('',*,*,#15880,.F.);
#22665=ORIENTED_EDGE('',*,*,#15881,.T.);
#22666=ORIENTED_EDGE('',*,*,#15872,.T.);
#22667=ORIENTED_EDGE('',*,*,#15881,.F.);
#22668=ORIENTED_EDGE('',*,*,#15882,.F.);
#22669=ORIENTED_EDGE('',*,*,#15883,.T.);
#22670=ORIENTED_EDGE('',*,*,#15873,.T.);
#22671=ORIENTED_EDGE('',*,*,#15883,.F.);
#22672=ORIENTED_EDGE('',*,*,#15884,.F.);
#22673=ORIENTED_EDGE('',*,*,#15885,.T.);
#22674=ORIENTED_EDGE('',*,*,#15874,.T.);
#22675=ORIENTED_EDGE('',*,*,#15885,.F.);
#22676=ORIENTED_EDGE('',*,*,#15886,.F.);
#22677=ORIENTED_EDGE('',*,*,#15875,.T.);
#22678=ORIENTED_EDGE('',*,*,#15876,.T.);
#22679=ORIENTED_EDGE('',*,*,#15886,.T.);
#22680=ORIENTED_EDGE('',*,*,#15884,.T.);
#22681=ORIENTED_EDGE('',*,*,#15882,.T.);
#22682=ORIENTED_EDGE('',*,*,#15880,.T.);
#22683=ORIENTED_EDGE('',*,*,#15878,.T.);
#23147=CYLINDRICAL_SURFACE('',#27371,5.);
#23148=CYLINDRICAL_SURFACE('',#27380,3.);
#24498=ADVANCED_FACE('',(#3506),#23147,.T.);
#24499=ADVANCED_FACE('',(#3507),#2155,.T.);
#24500=ADVANCED_FACE('',(#3508),#2156,.T.);
#24501=ADVANCED_FACE('',(#3509),#23148,.T.);
#24502=ADVANCED_FACE('',(#3510),#2085,.T.);
#24503=ADVANCED_FACE('',(#3511,#1338),#2086,.T.);
#24504=ADVANCED_FACE('',(#3512,#1339),#2087,.T.);
#24505=ADVANCED_FACE('',(#3513),#2088,.F.);
#24506=ADVANCED_FACE('',(#3514),#2089,.F.);
#24507=ADVANCED_FACE('',(#3515),#2090,.F.);
#24508=ADVANCED_FACE('',(#3516),#2091,.F.);
#24509=ADVANCED_FACE('',(#3517),#2092,.F.);
#24510=ADVANCED_FACE('',(#3518),#2093,.F.);
#24511=ADVANCED_FACE('',(#3519),#2094,.T.);
#24561=CLOSED_SHELL('',(#24498,#24499,#24500,#24501,#24502,#24503,#24504,
#24505,#24506,#24507,#24508,#24509,#24510,#24511));
#27370=AXIS2_PLACEMENT_3D('',#56813,#34374,#34375);
#27371=AXIS2_PLACEMENT_3D('',#56814,#34376,#34377);
#27372=AXIS2_PLACEMENT_3D('',#56816,#34378,#34379);
#27373=AXIS2_PLACEMENT_3D('',#56819,#34381,#34382);
#27374=AXIS2_PLACEMENT_3D('',#56820,#34383,#34384);
#27375=AXIS2_PLACEMENT_3D('',#56823,#34386,#34387);
#27376=AXIS2_PLACEMENT_3D('',#56824,#34388,#34389);
#27377=AXIS2_PLACEMENT_3D('',#56827,#34390,#34391);
#27378=AXIS2_PLACEMENT_3D('',#56830,#34393,#34394);
#27379=AXIS2_PLACEMENT_3D('',#56831,#34395,#34396);
#27380=AXIS2_PLACEMENT_3D('',#56832,#34397,#34398);
#27381=AXIS2_PLACEMENT_3D('',#56835,#34400,#34401);
#27382=AXIS2_PLACEMENT_3D('',#56836,#34402,#34403);
#27383=AXIS2_PLACEMENT_3D('',#56837,#34404,#34405);
#27384=AXIS2_PLACEMENT_3D('',#56850,#34412,#34413);
#27385=AXIS2_PLACEMENT_3D('',#56851,#34414,#34415);
#27386=AXIS2_PLACEMENT_3D('',#56857,#34419,#34420);
#27387=AXIS2_PLACEMENT_3D('',#56861,#34423,#34424);
#27388=AXIS2_PLACEMENT_3D('',#56865,#34427,#34428);
#27389=AXIS2_PLACEMENT_3D('',#56869,#34431,#34432);
#27390=AXIS2_PLACEMENT_3D('',#56873,#34435,#34436);
#27391=AXIS2_PLACEMENT_3D('',#56875,#34438,#34439);
#34374=DIRECTION('axis',(0.,0.,1.));
#34375=DIRECTION('refdir',(1.,0.,0.));
#34376=DIRECTION('center_axis',(1.,1.22464679914735E-16,0.));
#34377=DIRECTION('ref_axis',(-1.22464679914735E-16,1.,0.));
#34378=DIRECTION('center_axis',(1.,1.22464679914735E-16,0.));
#34379=DIRECTION('ref_axis',(-1.22464679914735E-16,1.,0.));
#34380=DIRECTION('',(-1.,-1.22464679914735E-16,0.));
#34381=DIRECTION('center_axis',(1.,1.22464679914735E-16,0.));
#34382=DIRECTION('ref_axis',(-1.22464679914735E-16,1.,0.));
#34383=DIRECTION('center_axis',(1.,1.22464679914735E-16,0.));
#34384=DIRECTION('ref_axis',(-1.22464679914735E-16,1.,0.));
#34385=DIRECTION('',(-0.70710678118655,0.707106781186545,8.6595605623549E-17));
#34386=DIRECTION('center_axis',(1.,1.22464679914735E-16,0.));
#34387=DIRECTION('ref_axis',(-1.22464679914735E-16,1.,0.));
#34388=DIRECTION('center_axis',(-1.,-1.22464679914735E-16,0.));
#34389=DIRECTION('ref_axis',(1.22464679914735E-16,-1.,0.));
#34390=DIRECTION('center_axis',(1.,1.22464679914735E-16,0.));
#34391=DIRECTION('ref_axis',(-1.22464679914735E-16,1.,0.));
#34392=DIRECTION('',(0.707106781186548,-0.707106781186547,8.65956056235493E-17));
#34393=DIRECTION('center_axis',(1.,1.22464679914735E-16,0.));
#34394=DIRECTION('ref_axis',(-1.22464679914735E-16,1.,0.));
#34395=DIRECTION('center_axis',(1.,1.22464679914735E-16,0.));
#34396=DIRECTION('ref_axis',(-1.22464679914735E-16,1.,0.));
#34397=DIRECTION('center_axis',(1.,1.22464679914735E-16,0.));
#34398=DIRECTION('ref_axis',(-1.22464679914735E-16,1.,0.));
#34399=DIRECTION('',(-1.,-1.22464679914735E-16,0.));
#34400=DIRECTION('center_axis',(1.,1.22464679914735E-16,0.));
#34401=DIRECTION('ref_axis',(-1.22464679914735E-16,1.,0.));
#34402=DIRECTION('center_axis',(1.,1.22464679914735E-16,0.));
#34403=DIRECTION('ref_axis',(-1.22464679914735E-16,1.,0.));
#34404=DIRECTION('center_axis',(-1.,-1.22464679914735E-16,0.));
#34405=DIRECTION('ref_axis',(1.22464679914735E-16,-1.,0.));
#34406=DIRECTION('',(0.,0.5,-0.866025403784439));
#34407=DIRECTION('',(0.,1.,0.));
#34408=DIRECTION('',(0.,0.5,0.866025403784439));
#34409=DIRECTION('',(0.,-0.5,0.866025403784438));
#34410=DIRECTION('',(0.,-1.,-1.50231459873716E-16));
#34411=DIRECTION('',(0.,-0.5,-0.866025403784439));
#34412=DIRECTION('center_axis',(1.,1.22464679914735E-16,0.));
#34413=DIRECTION('ref_axis',(-1.22464679914735E-16,1.,0.));
#34414=DIRECTION('center_axis',(-1.06057523872491E-16,0.866025403784439,
0.5));
#34415=DIRECTION('ref_axis',(-5.09861652542584E-33,-0.5,0.866025403784439));
#34416=DIRECTION('',(-1.,-1.22464679914735E-16,0.));
#34417=DIRECTION('',(0.,0.5,-0.866025403784439));
#34418=DIRECTION('',(-1.,-1.22464679914735E-16,0.));
#34419=DIRECTION('center_axis',(0.,0.,1.));
#34420=DIRECTION('ref_axis',(1.,0.,0.));
#34421=DIRECTION('',(0.,1.,0.));
#34422=DIRECTION('',(-1.,-1.22464679914735E-16,0.));
#34423=DIRECTION('center_axis',(1.06057523872491E-16,-0.866025403784439,
0.5));
#34424=DIRECTION('ref_axis',(-8.4117933897259E-34,-0.5,-0.866025403784439));
#34425=DIRECTION('',(0.,0.5,0.866025403784439));
#34426=DIRECTION('',(-1.,-1.22464679914735E-16,0.));
#34427=DIRECTION('center_axis',(1.06057523872491E-16,-0.866025403784439,
-0.5));
#34428=DIRECTION('ref_axis',(-5.93979586439842E-33,0.5,-0.866025403784439));
#34429=DIRECTION('',(0.,-0.5,0.866025403784438));
#34430=DIRECTION('',(-1.,-1.22464679914735E-16,0.));
#34431=DIRECTION('center_axis',(-1.8398047646558E-32,1.50231459873716E-16,
-1.));
#34432=DIRECTION('ref_axis',(0.,1.,1.50231459873716E-16));
#34433=DIRECTION('',(0.,-1.,-1.50231459873716E-16));
#34434=DIRECTION('',(-1.,-1.22464679914735E-16,0.));
#34435=DIRECTION('center_axis',(-1.06057523872491E-16,0.866025403784439,
-0.5));
#34436=DIRECTION('ref_axis',(2.96989793219921E-33,0.5,0.866025403784439));
#34437=DIRECTION('',(0.,-0.5,-0.866025403784439));
#34438=DIRECTION('center_axis',(-1.,0.,0.));
#34439=DIRECTION('ref_axis',(0.,0.,1.));
#56813=CARTESIAN_POINT('',(0.,0.,0.));
#56814=CARTESIAN_POINT('Origin',(20.,1.71450551880629E-15,0.));
#56815=CARTESIAN_POINT('',(0.,-5.,-6.12323399573677E-16));
#56816=CARTESIAN_POINT('Origin',(0.,-7.34788079488412E-16,0.));
#56817=CARTESIAN_POINT('',(-5.4,-5.,-6.12323399573677E-16));
#56818=CARTESIAN_POINT('',(20.,-5.,-6.12323399573677E-16));
#56819=CARTESIAN_POINT('Origin',(-5.4,-1.39609735102798E-15,0.));
#56820=CARTESIAN_POINT('Origin',(-5.4,-1.39609735102798E-15,0.));
#56821=CARTESIAN_POINT('',(-6.,-4.4,-5.38844591624836E-16));
#56822=CARTESIAN_POINT('',(-5.4,-5.,-6.12323399573677E-16));
#56823=CARTESIAN_POINT('Origin',(-6.,-1.46957615897682E-15,0.));
#56824=CARTESIAN_POINT('Origin',(20.,1.71450551880629E-15,0.));
#56825=CARTESIAN_POINT('',(19.4585,-3.,3.67394039744206E-16));
#56826=CARTESIAN_POINT('',(19.4585,3.,-3.67394039744206E-16));
#56827=CARTESIAN_POINT('Origin',(19.4585,1.64819089463247E-15,0.));
#56828=CARTESIAN_POINT('',(20.,2.4585,-3.01079415570377E-16));
#56829=CARTESIAN_POINT('',(20.,2.4585,-3.01079415570377E-16));
#56830=CARTESIAN_POINT('Origin',(20.,1.71450551880629E-15,0.));
#56831=CARTESIAN_POINT('Origin',(19.4585,1.64819089463247E-15,0.));
#56832=CARTESIAN_POINT('Origin',(20.,1.71450551880629E-15,0.));
#56833=CARTESIAN_POINT('',(0.,-3.,-3.67394039744206E-16));
#56834=CARTESIAN_POINT('',(20.,-3.,-3.67394039744206E-16));
#56835=CARTESIAN_POINT('Origin',(0.,-7.34788079488412E-16,0.));
#56836=CARTESIAN_POINT('Origin',(20.,2.4585,0.));
#56837=CARTESIAN_POINT('Origin',(-6.,-1.46957615897682E-15,0.));
#56838=CARTESIAN_POINT('',(-6.,1.44337567297406,2.5));
#56839=CARTESIAN_POINT('',(-6.,2.88675134594813,0.));
#56840=CARTESIAN_POINT('',(-6.,1.44337567297406,2.5));
#56841=CARTESIAN_POINT('',(-6.,-1.44337567297407,2.5));
#56842=CARTESIAN_POINT('',(-6.,-1.44337567297407,2.5));
#56843=CARTESIAN_POINT('',(-6.,-2.88675134594813,-7.77133304087269E-16));
#56844=CARTESIAN_POINT('',(-6.,-2.88675134594813,-7.77133304087269E-16));
#56845=CARTESIAN_POINT('',(-6.,-1.44337567297407,-2.5));
#56846=CARTESIAN_POINT('',(-6.,-1.44337567297407,-2.5));
#56847=CARTESIAN_POINT('',(-6.,1.44337567297406,-2.5));
#56848=CARTESIAN_POINT('',(-6.,1.44337567297406,-2.5));
#56849=CARTESIAN_POINT('',(-6.,2.88675134594813,3.50584097974525E-17));
#56850=CARTESIAN_POINT('Origin',(1.22464679914735E-16,3.,0.));
#56851=CARTESIAN_POINT('Origin',(-3.,1.44337567297406,2.5));
#56852=CARTESIAN_POINT('',(-3.,2.88675134594813,3.50584097974525E-17));
#56853=CARTESIAN_POINT('',(-3.,2.88675134594813,3.50584097974525E-17));
#56854=CARTESIAN_POINT('',(-3.,1.44337567297406,2.5));
#56855=CARTESIAN_POINT('',(-3.,1.44337567297406,2.5));
#56856=CARTESIAN_POINT('',(-3.,1.44337567297406,2.5));
#56857=CARTESIAN_POINT('Origin',(-3.,-1.44337567297407,2.5));
#56858=CARTESIAN_POINT('',(-3.,-1.44337567297407,2.5));
#56859=CARTESIAN_POINT('',(-3.,-1.44337567297407,2.5));
#56860=CARTESIAN_POINT('',(-3.,-1.44337567297407,2.5));
#56861=CARTESIAN_POINT('Origin',(-3.,-2.88675134594813,-7.77133304087269E-16));
#56862=CARTESIAN_POINT('',(-3.,-2.88675134594813,-7.77133304087269E-16));
#56863=CARTESIAN_POINT('',(-3.,-2.88675134594813,-7.77133304087269E-16));
#56864=CARTESIAN_POINT('',(-3.,-2.88675134594813,-7.77133304087269E-16));
#56865=CARTESIAN_POINT('Origin',(-3.,-1.44337567297406,-2.5));
#56866=CARTESIAN_POINT('',(-3.,-1.44337567297406,-2.5));
#56867=CARTESIAN_POINT('',(-3.,-1.44337567297406,-2.5));
#56868=CARTESIAN_POINT('',(-3.,-1.44337567297406,-2.5));
#56869=CARTESIAN_POINT('Origin',(-3.,1.44337567297407,-2.5));
#56870=CARTESIAN_POINT('',(-3.,1.44337567297407,-2.5));
#56871=CARTESIAN_POINT('',(-3.,1.44337567297407,-2.5));
#56872=CARTESIAN_POINT('',(-3.,1.44337567297407,-2.5));
#56873=CARTESIAN_POINT('Origin',(-3.,2.88675134594813,3.50584097974525E-17));
#56874=CARTESIAN_POINT('',(-3.,2.88675134594813,3.50584097974525E-17));
#56875=CARTESIAN_POINT('Origin',(-3.,3.67394039744206E-16,0.));
#57038=UNCERTAINTY_MEASURE_WITH_UNIT(LENGTH_MEASURE(0.01),#57080,
'DISTANCE_ACCURACY_VALUE',
'Maximum model space distance between geometric entities at asserted c
onnectivities');
#57040=UNCERTAINTY_MEASURE_WITH_UNIT(LENGTH_MEASURE(0.01),#57080,
'DISTANCE_ACCURACY_VALUE',
'Maximum model space distance between geometric entities at asserted c
onnectivities');
#57077=(
GEOMETRIC_REPRESENTATION_CONTEXT(3)
GLOBAL_UNCERTAINTY_ASSIGNED_CONTEXT((#57038))
GLOBAL_UNIT_ASSIGNED_CONTEXT((#57080,#57082,#57083))
REPRESENTATION_CONTEXT('','3D')
);
#57079=(
GEOMETRIC_REPRESENTATION_CONTEXT(3)
GLOBAL_UNCERTAINTY_ASSIGNED_CONTEXT((#57040))
GLOBAL_UNIT_ASSIGNED_CONTEXT((#57080,#57082,#57083))
REPRESENTATION_CONTEXT('','3D')
);
#57080=(
LENGTH_UNIT()
NAMED_UNIT(*)
SI_UNIT(.MILLI.,.METRE.)
);
#57082=(
NAMED_UNIT(*)
PLANE_ANGLE_UNIT()
SI_UNIT($,.RADIAN.)
);
#57083=(
NAMED_UNIT(*)
SI_UNIT($,.STERADIAN.)
SOLID_ANGLE_UNIT()
);
#57120=SHAPE_DEFINITION_REPRESENTATION(#57184,#57285);
#57184=PRODUCT_DEFINITION_SHAPE('',$,#57324);
#57285=SHAPE_REPRESENTATION('',(#27370),#57077);
#57287=PRODUCT_DEFINITION_CONTEXT('part definition',#57403,'design');
#57324=PRODUCT_DEFINITION('Socket head cap screw M6x20',
'Socket Head Cap Screw M6x20',#57362,#57287);
#57362=PRODUCT_DEFINITION_FORMATION('',$,#57441);
#57403=APPLICATION_CONTEXT(
'Core Data for Automotive Mechanical Design Process');
#57404=PRODUCT_CONTEXT('part definition',#57403,'mechanical');
#57441=PRODUCT('Socket head cap screw M6x20',
'Socket Head Cap Screw M6x20',$,(#57404));
#57444=PRESENTATION_STYLE_ASSIGNMENT((#57446));
#57446=SURFACE_STYLE_USAGE(.BOTH.,#57448);
#57448=SURFACE_SIDE_STYLE('',(#57450));
#57450=SURFACE_STYLE_FILL_AREA(#57452);
#57452=FILL_AREA_STYLE('Opaque(202,209,238)',(#57454));
#57454=FILL_AREA_STYLE_COLOUR('Opaque(202,209,238)',#57456);
#57456=COLOUR_RGB('Opaque(202,209,238)',0.792156862745098,0.819607843137255,
0.933333333333333);
ENDSEC;
END-ISO-10303-21;
